ISO-10303-21;
HEADER;
/* Generated by software containing ST-Developer
 * from STEP Tools, Inc. (www.steptools.com) 
 */

FILE_DESCRIPTION(
/* description */ ('Grid plate located blocks and clamp'),
/* implementation_level */ '2;1');

FILE_NAME(
/* name */ 'Hex Nut - M8.step',
/* time_stamp */ '2026-10-29T15:43:47-07:00',
/* author */ (''),
/* organization */ (''),
/* preprocessor_version */ 'ST-DEVELOPER v20.2',
/* originating_system */ 'Autodesk Translation Framework v15.17.0.0',
/* authorisation */ '');

FILE_SCHEMA (('AUTOMOTIVE_DESIGN { 1 0 10303 214 3 1 1 }'));
ENDSEC;

DATA;
#10=MECHANICAL_DESIGN_GEOMETRIC_PRESENTATION_REPRESENTATION('',(#178),#5702);
#115=(
BOUNDED_CURVE()
B_SPLINE_CURVE(2,(#5458,#5459,#5460),.UNSPECIFIED.,.F.,.F.)
B_SPLINE_CURVE_WITH_KNOTS((3,3),(0.14973948338295,0.97160236658079),
 .UNSPECIFIED.)
CURVE()
GEOMETRIC_REPRESENTATION_ITEM()
RATIONAL_B_SPLINE_CURVE((1.07140024848292,1.23714644374248,1.07140024848292))
REPRESENTATION_ITEM('')
);
#116=(
BOUNDED_CURVE()
B_SPLINE_CURVE(2,(#5462,#5463,#5464),.UNSPECIFIED.,.F.,.F.)
B_SPLINE_CURVE_WITH_KNOTS((3,3),(0.14973948338295,0.971602366580789),
 .UNSPECIFIED.)
CURVE()
GEOMETRIC_REPRESENTATION_ITEM()
RATIONAL_B_SPLINE_CURVE((1.07140024848292,1.23714644374248,1.07140024848292))
REPRESENTATION_ITEM('')
);
#117=(
BOUNDED_CURVE()
B_SPLINE_CURVE(2,(#5469,#5470,#5471),.UNSPECIFIED.,.F.,.F.)
B_SPLINE_CURVE_WITH_KNOTS((3,3),(0.14973948338295,0.97160236658079),
 .UNSPECIFIED.)
CURVE()
GEOMETRIC_REPRESENTATION_ITEM()
RATIONAL_B_SPLINE_CURVE((1.07140024848292,1.23714644374248,1.07140024848292))
REPRESENTATION_ITEM('')
);
#118=(
BOUNDED_CURVE()
B_SPLINE_CURVE(2,(#5473,#5474,#5475),.UNSPECIFIED.,.F.,.F.)
B_SPLINE_CURVE_WITH_KNOTS((3,3),(0.14973948338295,0.97160236658079),
 .UNSPECIFIED.)
CURVE()
GEOMETRIC_REPRESENTATION_ITEM()
RATIONAL_B_SPLINE_CURVE((1.07140024848292,1.23714644374248,1.07140024848292))
REPRESENTATION_ITEM('')
);
#119=(
BOUNDED_CURVE()
B_SPLINE_CURVE(2,(#5477,#5478,#5479),.UNSPECIFIED.,.F.,.F.)
B_SPLINE_CURVE_WITH_KNOTS((3,3),(0.14973948338295,0.971602366580789),
 .UNSPECIFIED.)
CURVE()
GEOMETRIC_REPRESENTATION_ITEM()
RATIONAL_B_SPLINE_CURVE((1.07140024848292,1.23714644374248,1.07140024848292))
REPRESENTATION_ITEM('')
);
#120=(
BOUNDED_CURVE()
B_SPLINE_CURVE(2,(#5480,#5481,#5482),.UNSPECIFIED.,.F.,.F.)
B_SPLINE_CURVE_WITH_KNOTS((3,3),(0.14973948338295,0.97160236658079),
 .UNSPECIFIED.)
CURVE()
GEOMETRIC_REPRESENTATION_ITEM()
RATIONAL_B_SPLINE_CURVE((1.07140024848292,1.23714644374248,1.07140024848292))
REPRESENTATION_ITEM('')
);
#121=(
BOUNDED_CURVE()
B_SPLINE_CURVE(2,(#5489,#5490,#5491),.UNSPECIFIED.,.F.,.F.)
B_SPLINE_CURVE_WITH_KNOTS((3,3),(0.14973948338295,0.97160236658079),
 .UNSPECIFIED.)
CURVE()
GEOMETRIC_REPRESENTATION_ITEM()
RATIONAL_B_SPLINE_CURVE((1.07140024848292,1.23714644374248,1.07140024848292))
REPRESENTATION_ITEM('')
);
#122=(
BOUNDED_CURVE()
B_SPLINE_CURVE(2,(#5493,#5494,#5495),.UNSPECIFIED.,.F.,.F.)
B_SPLINE_CURVE_WITH_KNOTS((3,3),(0.14973948338295,0.97160236658079),
 .UNSPECIFIED.)
CURVE()
GEOMETRIC_REPRESENTATION_ITEM()
RATIONAL_B_SPLINE_CURVE((1.07140024848292,1.23714644374248,1.07140024848292))
REPRESENTATION_ITEM('')
);
#123=(
BOUNDED_CURVE()
B_SPLINE_CURVE(2,(#5497,#5498,#5499),.UNSPECIFIED.,.F.,.F.)
B_SPLINE_CURVE_WITH_KNOTS((3,3),(0.14973948338295,0.971602366580789),
 .UNSPECIFIED.)
CURVE()
GEOMETRIC_REPRESENTATION_ITEM()
RATIONAL_B_SPLINE_CURVE((1.07140024848292,1.23714644374248,1.07140024848292))
REPRESENTATION_ITEM('')
);
#124=(
BOUNDED_CURVE()
B_SPLINE_CURVE(2,(#5501,#5502,#5503),.UNSPECIFIED.,.F.,.F.)
B_SPLINE_CURVE_WITH_KNOTS((3,3),(0.14973948338295,0.97160236658079),
 .UNSPECIFIED.)
CURVE()
GEOMETRIC_REPRESENTATION_ITEM()
RATIONAL_B_SPLINE_CURVE((1.07140024848292,1.23714644374248,1.07140024848292))
REPRESENTATION_ITEM('')
);
#125=(
BOUNDED_CURVE()
B_SPLINE_CURVE(2,(#5505,#5506,#5507),.UNSPECIFIED.,.F.,.F.)
B_SPLINE_CURVE_WITH_KNOTS((3,3),(0.14973948338295,0.97160236658079),
 .UNSPECIFIED.)
CURVE()
GEOMETRIC_REPRESENTATION_ITEM()
RATIONAL_B_SPLINE_CURVE((1.07140024848292,1.23714644374248,1.07140024848292))
REPRESENTATION_ITEM('')
);
#126=(
BOUNDED_CURVE()
B_SPLINE_CURVE(2,(#5508,#5509,#5510),.UNSPECIFIED.,.F.,.F.)
B_SPLINE_CURVE_WITH_KNOTS((3,3),(0.14973948338295,0.971602366580789),
 .UNSPECIFIED.)
CURVE()
GEOMETRIC_REPRESENTATION_ITEM()
RATIONAL_B_SPLINE_CURVE((1.07140024848292,1.23714644374248,1.07140024848292))
REPRESENTATION_ITEM('')
);
#136=CONICAL_SURFACE('',#3673,0.734027674973257,1.0471975511966);
#137=CONICAL_SURFACE('',#3675,0.734027674973257,1.0471975511966);
#152=SHAPE_REPRESENTATION_RELATIONSHIP('SRR','None',#5770,#164);
#164=ADVANCED_BREP_SHAPE_REPRESENTATION('',(#190),#5700);
#178=STYLED_ITEM('',(#5904),#190);
#190=MANIFOLD_SOLID_BREP('Body1',#3275);
#263=FACE_BOUND('',#871,.T.);
#264=FACE_BOUND('',#873,.T.);
#367=CIRCLE('',#3674,0.6175);
#368=CIRCLE('',#3676,0.6175);
#369=CIRCLE('',#3681,0.338975);
#370=CIRCLE('',#3682,0.338975);
#443=CYLINDRICAL_SURFACE('',#3680,0.338975);
#607=FACE_OUTER_BOUND('',#861,.T.);
#608=FACE_OUTER_BOUND('',#862,.T.);
#609=FACE_OUTER_BOUND('',#863,.T.);
#610=FACE_OUTER_BOUND('',#864,.T.);
#611=FACE_OUTER_BOUND('',#865,.T.);
#612=FACE_OUTER_BOUND('',#866,.T.);
#613=FACE_OUTER_BOUND('',#867,.T.);
#614=FACE_OUTER_BOUND('',#868,.T.);
#615=FACE_OUTER_BOUND('',#869,.T.);
#616=FACE_OUTER_BOUND('',#870,.T.);
#617=FACE_OUTER_BOUND('',#872,.T.);
#861=EDGE_LOOP('',(#2800,#2801,#2802,#2803,#2804,#2805,#2806,#2807,#2808));
#862=EDGE_LOOP('',(#2809,#2810,#2811,#2812,#2813,#2814,#2815,#2816,#2817));
#863=EDGE_LOOP('',(#2818,#2819,#2820,#2821));
#864=EDGE_LOOP('',(#2822,#2823,#2824,#2825));
#865=EDGE_LOOP('',(#2826,#2827,#2828,#2829));
#866=EDGE_LOOP('',(#2830,#2831,#2832,#2833));
#867=EDGE_LOOP('',(#2834,#2835,#2836,#2837));
#868=EDGE_LOOP('',(#2838,#2839,#2840,#2841));
#869=EDGE_LOOP('',(#2842,#2843,#2844,#2845));
#870=EDGE_LOOP('',(#2846));
#871=EDGE_LOOP('',(#2847));
#872=EDGE_LOOP('',(#2848));
#873=EDGE_LOOP('',(#2849));
#1132=LINE('',#5466,#1405);
#1133=LINE('',#5487,#1406);
#1134=LINE('',#5512,#1407);
#1135=LINE('',#5513,#1408);
#1136=LINE('',#5515,#1409);
#1137=LINE('',#5517,#1410);
#1138=LINE('',#5522,#1411);
#1139=LINE('',#5525,#1412);
#1140=LINE('',#5527,#1413);
#1405=VECTOR('',#4524,0.734027674973257);
#1406=VECTOR('',#4531,0.734027674973257);
#1407=VECTOR('',#4534,1.);
#1408=VECTOR('',#4535,1.);
#1409=VECTOR('',#4538,1.);
#1410=VECTOR('',#4541,1.);
#1411=VECTOR('',#4546,0.4);
#1412=VECTOR('',#4551,1.);
#1413=VECTOR('',#4554,1.);
#1662=VERTEX_POINT('',#5456);
#1663=VERTEX_POINT('',#5457);
#1664=VERTEX_POINT('',#5461);
#1665=VERTEX_POINT('',#5465);
#1666=VERTEX_POINT('',#5468);
#1667=VERTEX_POINT('',#5472);
#1668=VERTEX_POINT('',#5476);
#1669=VERTEX_POINT('',#5484);
#1670=VERTEX_POINT('',#5486);
#1671=VERTEX_POINT('',#5488);
#1672=VERTEX_POINT('',#5492);
#1673=VERTEX_POINT('',#5496);
#1674=VERTEX_POINT('',#5500);
#1675=VERTEX_POINT('',#5504);
#1676=VERTEX_POINT('',#5519);
#1677=VERTEX_POINT('',#5521);
#2050=EDGE_CURVE('',#1662,#1663,#115,.T.);
#2051=EDGE_CURVE('',#1664,#1662,#116,.T.);
#2052=EDGE_CURVE('',#1664,#1665,#1132,.T.);
#2053=EDGE_CURVE('',#1665,#1665,#367,.T.);
#2054=EDGE_CURVE('',#1666,#1664,#117,.T.);
#2055=EDGE_CURVE('',#1667,#1666,#118,.T.);
#2056=EDGE_CURVE('',#1668,#1667,#119,.T.);
#2057=EDGE_CURVE('',#1663,#1668,#120,.T.);
#2058=EDGE_CURVE('',#1669,#1669,#368,.T.);
#2059=EDGE_CURVE('',#1669,#1670,#1133,.T.);
#2060=EDGE_CURVE('',#1671,#1670,#121,.T.);
#2061=EDGE_CURVE('',#1672,#1671,#122,.T.);
#2062=EDGE_CURVE('',#1673,#1672,#123,.T.);
#2063=EDGE_CURVE('',#1674,#1673,#124,.T.);
#2064=EDGE_CURVE('',#1675,#1674,#125,.T.);
#2065=EDGE_CURVE('',#1670,#1675,#126,.T.);
#2066=EDGE_CURVE('',#1666,#1675,#1134,.T.);
#2067=EDGE_CURVE('',#1667,#1674,#1135,.T.);
#2068=EDGE_CURVE('',#1664,#1670,#1136,.T.);
#2069=EDGE_CURVE('',#1662,#1671,#1137,.T.);
#2070=EDGE_CURVE('',#1676,#1676,#369,.F.);
#2071=EDGE_CURVE('',#1676,#1677,#1138,.T.);
#2072=EDGE_CURVE('',#1677,#1677,#370,.F.);
#2073=EDGE_CURVE('',#1663,#1672,#1139,.T.);
#2074=EDGE_CURVE('',#1668,#1673,#1140,.T.);
#2800=ORIENTED_EDGE('',*,*,#2050,.F.);
#2801=ORIENTED_EDGE('',*,*,#2051,.F.);
#2802=ORIENTED_EDGE('',*,*,#2052,.T.);
#2803=ORIENTED_EDGE('',*,*,#2053,.F.);
#2804=ORIENTED_EDGE('',*,*,#2052,.F.);
#2805=ORIENTED_EDGE('',*,*,#2054,.F.);
#2806=ORIENTED_EDGE('',*,*,#2055,.F.);
#2807=ORIENTED_EDGE('',*,*,#2056,.F.);
#2808=ORIENTED_EDGE('',*,*,#2057,.F.);
#2809=ORIENTED_EDGE('',*,*,#2058,.F.);
#2810=ORIENTED_EDGE('',*,*,#2059,.T.);
#2811=ORIENTED_EDGE('',*,*,#2060,.F.);
#2812=ORIENTED_EDGE('',*,*,#2061,.F.);
#2813=ORIENTED_EDGE('',*,*,#2062,.F.);
#2814=ORIENTED_EDGE('',*,*,#2063,.F.);
#2815=ORIENTED_EDGE('',*,*,#2064,.F.);
#2816=ORIENTED_EDGE('',*,*,#2065,.F.);
#2817=ORIENTED_EDGE('',*,*,#2059,.F.);
#2818=ORIENTED_EDGE('',*,*,#2055,.T.);
#2819=ORIENTED_EDGE('',*,*,#2066,.T.);
#2820=ORIENTED_EDGE('',*,*,#2064,.T.);
#2821=ORIENTED_EDGE('',*,*,#2067,.F.);
#2822=ORIENTED_EDGE('',*,*,#2054,.T.);
#2823=ORIENTED_EDGE('',*,*,#2068,.T.);
#2824=ORIENTED_EDGE('',*,*,#2065,.T.);
#2825=ORIENTED_EDGE('',*,*,#2066,.F.);
#2826=ORIENTED_EDGE('',*,*,#2051,.T.);
#2827=ORIENTED_EDGE('',*,*,#2069,.T.);
#2828=ORIENTED_EDGE('',*,*,#2060,.T.);
#2829=ORIENTED_EDGE('',*,*,#2068,.F.);
#2830=ORIENTED_EDGE('',*,*,#2070,.F.);
#2831=ORIENTED_EDGE('',*,*,#2071,.T.);
#2832=ORIENTED_EDGE('',*,*,#2072,.T.);
#2833=ORIENTED_EDGE('',*,*,#2071,.F.);
#2834=ORIENTED_EDGE('',*,*,#2050,.T.);
#2835=ORIENTED_EDGE('',*,*,#2073,.T.);
#2836=ORIENTED_EDGE('',*,*,#2061,.T.);
#2837=ORIENTED_EDGE('',*,*,#2069,.F.);
#2838=ORIENTED_EDGE('',*,*,#2056,.T.);
#2839=ORIENTED_EDGE('',*,*,#2067,.T.);
#2840=ORIENTED_EDGE('',*,*,#2063,.T.);
#2841=ORIENTED_EDGE('',*,*,#2074,.F.);
#2842=ORIENTED_EDGE('',*,*,#2057,.T.);
#2843=ORIENTED_EDGE('',*,*,#2074,.T.);
#2844=ORIENTED_EDGE('',*,*,#2062,.T.);
#2845=ORIENTED_EDGE('',*,*,#2073,.F.);
#2846=ORIENTED_EDGE('',*,*,#2058,.T.);
#2847=ORIENTED_EDGE('',*,*,#2070,.T.);
#2848=ORIENTED_EDGE('',*,*,#2053,.T.);
#2849=ORIENTED_EDGE('',*,*,#2072,.F.);
#3061=PLANE('',#3677);
#3062=PLANE('',#3678);
#3063=PLANE('',#3679);
#3064=PLANE('',#3683);
#3065=PLANE('',#3684);
#3066=PLANE('',#3685);
#3067=PLANE('',#3686);
#3068=PLANE('',#3687);
#3228=ADVANCED_FACE('',(#607),#136,.T.);
#3229=ADVANCED_FACE('',(#608),#137,.T.);
#3230=ADVANCED_FACE('',(#609),#3061,.T.);
#3231=ADVANCED_FACE('',(#610),#3062,.T.);
#3232=ADVANCED_FACE('',(#611),#3063,.T.);
#3233=ADVANCED_FACE('',(#612),#443,.F.);
#3234=ADVANCED_FACE('',(#613),#3064,.T.);
#3235=ADVANCED_FACE('',(#614),#3065,.T.);
#3236=ADVANCED_FACE('',(#615),#3066,.T.);
#3237=ADVANCED_FACE('',(#616,#263),#3067,.T.);
#3238=ADVANCED_FACE('',(#617,#264),#3068,.F.);
#3275=CLOSED_SHELL('',(#3228,#3229,#3230,#3231,#3232,#3233,#3234,#3235,
#3236,#3237,#3238));
#3672=AXIS2_PLACEMENT_3D('',#5454,#4520,#4521);
#3673=AXIS2_PLACEMENT_3D('',#5455,#4522,#4523);
#3674=AXIS2_PLACEMENT_3D('',#5467,#4525,#4526);
#3675=AXIS2_PLACEMENT_3D('',#5483,#4527,#4528);
#3676=AXIS2_PLACEMENT_3D('',#5485,#4529,#4530);
#3677=AXIS2_PLACEMENT_3D('',#5511,#4532,#4533);
#3678=AXIS2_PLACEMENT_3D('',#5514,#4536,#4537);
#3679=AXIS2_PLACEMENT_3D('',#5516,#4539,#4540);
#3680=AXIS2_PLACEMENT_3D('',#5518,#4542,#4543);
#3681=AXIS2_PLACEMENT_3D('',#5520,#4544,#4545);
#3682=AXIS2_PLACEMENT_3D('',#5523,#4547,#4548);
#3683=AXIS2_PLACEMENT_3D('',#5524,#4549,#4550);
#3684=AXIS2_PLACEMENT_3D('',#5526,#4552,#4553);
#3685=AXIS2_PLACEMENT_3D('',#5528,#4555,#4556);
#3686=AXIS2_PLACEMENT_3D('',#5529,#4557,#4558);
#3687=AXIS2_PLACEMENT_3D('',#5530,#4559,#4560);
#4520=DIRECTION('axis',(0.,0.,1.));
#4521=DIRECTION('refdir',(1.,0.,0.));
#4522=DIRECTION('center_axis',(0.,1.,0.));
#4523=DIRECTION('ref_axis',(1.,0.,0.));
#4524=DIRECTION('',(0.866025403784439,-0.5,1.06057523872491E-16));
#4525=DIRECTION('center_axis',(0.,-1.,0.));
#4526=DIRECTION('ref_axis',(1.,0.,0.));
#4527=DIRECTION('center_axis',(0.,-1.,0.));
#4528=DIRECTION('ref_axis',(1.,0.,0.));
#4529=DIRECTION('center_axis',(0.,1.,0.));
#4530=DIRECTION('ref_axis',(1.,0.,0.));
#4531=DIRECTION('',(-0.866025403784439,-0.5,-1.06057523872491E-16));
#4532=DIRECTION('center_axis',(1.4792020664489E-16,0.,-1.));
#4533=DIRECTION('ref_axis',(-1.,0.,-1.4792020664489E-16));
#4534=DIRECTION('',(0.,1.,0.));
#4535=DIRECTION('',(0.,1.,0.));
#4536=DIRECTION('center_axis',(-0.866025403784439,0.,-0.5));
#4537=DIRECTION('ref_axis',(-0.5,0.,0.866025403784439));
#4538=DIRECTION('',(0.,1.,0.));
#4539=DIRECTION('center_axis',(-0.866025403784439,0.,0.5));
#4540=DIRECTION('ref_axis',(0.5,0.,0.866025403784439));
#4541=DIRECTION('',(0.,1.,0.));
#4542=DIRECTION('center_axis',(0.,1.,0.));
#4543=DIRECTION('ref_axis',(1.,0.,0.));
#4544=DIRECTION('center_axis',(0.,1.,0.));
#4545=DIRECTION('ref_axis',(1.,0.,0.));
#4546=DIRECTION('',(0.,-1.,0.));
#4547=DIRECTION('center_axis',(0.,1.,0.));
#4548=DIRECTION('ref_axis',(1.,0.,0.));
#4549=DIRECTION('center_axis',(-2.95840413289779E-16,0.,1.));
#4550=DIRECTION('ref_axis',(1.,0.,2.95840413289779E-16));
#4551=DIRECTION('',(0.,1.,0.));
#4552=DIRECTION('center_axis',(0.866025403784439,0.,-0.5));
#4553=DIRECTION('ref_axis',(-0.5,0.,-0.866025403784439));
#4554=DIRECTION('',(0.,1.,0.));
#4555=DIRECTION('center_axis',(0.866025403784439,0.,0.5));
#4556=DIRECTION('ref_axis',(0.5,0.,-0.866025403784439));
#4557=DIRECTION('center_axis',(0.,1.,0.));
#4558=DIRECTION('ref_axis',(1.,0.,0.));
#4559=DIRECTION('center_axis',(0.,1.,0.));
#4560=DIRECTION('ref_axis',(1.,0.,0.));
#5454=CARTESIAN_POINT('',(0.,0.,0.));
#5455=CARTESIAN_POINT('Origin',(0.,0.067277284513851,0.));
#5456=CARTESIAN_POINT('',(-0.375277674973257,0.0768195421087395,0.65));
#5457=CARTESIAN_POINT('',(0.375277674973257,0.0768195421087395,0.65));
#5458=CARTESIAN_POINT('Ctrl Pts',(-0.375277674973257,0.0768195421087395,
0.65));
#5459=CARTESIAN_POINT('Ctrl Pts',(1.66533453693773E-13,-0.0315137912242439,
0.65));
#5460=CARTESIAN_POINT('Ctrl Pts',(0.375277674973257,0.0768195421087394,
0.65));
#5461=CARTESIAN_POINT('',(-0.750555349946514,0.0768195421087394,-9.19165206894919E-17));
#5462=CARTESIAN_POINT('Ctrl Pts',(-0.750555349946514,0.0768195421087394,
-9.19165206894919E-17));
#5463=CARTESIAN_POINT('Ctrl Pts',(-0.562916512459802,-0.0315137912242434,
0.325000000000144));
#5464=CARTESIAN_POINT('Ctrl Pts',(-0.375277674973257,0.0768195421087395,
0.65));
#5465=CARTESIAN_POINT('',(-0.6175,-2.77555756156289E-17,-7.5621939847349E-17));
#5466=CARTESIAN_POINT('',(-0.734027674973257,0.067277284513851,-8.98924642641573E-17));
#5467=CARTESIAN_POINT('Origin',(0.,0.,0.));
#5468=CARTESIAN_POINT('',(-0.375277674973257,0.0768195421087395,-0.65));
#5469=CARTESIAN_POINT('Ctrl Pts',(-0.375277674973257,0.0768195421087395,
-0.65));
#5470=CARTESIAN_POINT('Ctrl Pts',(-0.562916512459968,-0.0315137912242437,
-0.324999999999856));
#5471=CARTESIAN_POINT('Ctrl Pts',(-0.750555349946514,0.0768195421087395,
-9.19165206894919E-17));
#5472=CARTESIAN_POINT('',(0.375277674973257,0.0768195421087395,-0.65));
#5473=CARTESIAN_POINT('Ctrl Pts',(0.375277674973257,0.0768195421087395,
-0.65));
#5474=CARTESIAN_POINT('Ctrl Pts',(-1.66144875635155E-13,-0.0315137912242437,
-0.65));
#5475=CARTESIAN_POINT('Ctrl Pts',(-0.375277674973257,0.0768195421087395,
-0.65));
#5476=CARTESIAN_POINT('',(0.750555349946514,0.0768195421087394,0.));
#5477=CARTESIAN_POINT('Ctrl Pts',(0.750555349946514,0.0768195421087394,
0.));
#5478=CARTESIAN_POINT('Ctrl Pts',(0.562916512459802,-0.0315137912242436,
-0.325000000000144));
#5479=CARTESIAN_POINT('Ctrl Pts',(0.375277674973257,0.0768195421087395,
-0.65));
#5480=CARTESIAN_POINT('Ctrl Pts',(0.375277674973257,0.0768195421087394,
0.65));
#5481=CARTESIAN_POINT('Ctrl Pts',(0.562916512459968,-0.0315137912242439,
0.324999999999856));
#5482=CARTESIAN_POINT('Ctrl Pts',(0.750555349946514,0.0768195421087394,
0.));
#5483=CARTESIAN_POINT('Origin',(0.,0.612722715486149,0.));
#5484=CARTESIAN_POINT('',(-0.6175,0.68,-7.5621939847349E-17));
#5485=CARTESIAN_POINT('Origin',(0.,0.68,0.));
#5486=CARTESIAN_POINT('',(-0.750555349946514,0.603180457891261,-9.19165206894919E-17));
#5487=CARTESIAN_POINT('',(-0.734027674973257,0.612722715486149,-8.98924642641573E-17));
#5488=CARTESIAN_POINT('',(-0.375277674973257,0.603180457891261,0.65));
#5489=CARTESIAN_POINT('Ctrl Pts',(-0.375277674973257,0.603180457891261,
0.65));
#5490=CARTESIAN_POINT('Ctrl Pts',(-0.562916512459968,0.711513791224243,
0.324999999999856));
#5491=CARTESIAN_POINT('Ctrl Pts',(-0.750555349946514,0.603180457891261,
-9.19165206894919E-17));
#5492=CARTESIAN_POINT('',(0.375277674973257,0.603180457891261,0.65));
#5493=CARTESIAN_POINT('Ctrl Pts',(0.375277674973257,0.603180457891261,0.65));
#5494=CARTESIAN_POINT('Ctrl Pts',(-1.66755498298699E-13,0.711513791224244,
0.65));
#5495=CARTESIAN_POINT('Ctrl Pts',(-0.375277674973257,0.603180457891261,
0.65));
#5496=CARTESIAN_POINT('',(0.750555349946514,0.603180457891261,0.));
#5497=CARTESIAN_POINT('Ctrl Pts',(0.750555349946514,0.603180457891261,0.));
#5498=CARTESIAN_POINT('Ctrl Pts',(0.562916512459802,0.711513791224244,0.325000000000144));
#5499=CARTESIAN_POINT('Ctrl Pts',(0.375277674973257,0.603180457891261,0.65));
#5500=CARTESIAN_POINT('',(0.375277674973257,0.603180457891261,-0.65));
#5501=CARTESIAN_POINT('Ctrl Pts',(0.375277674973257,0.603180457891261,-0.65));
#5502=CARTESIAN_POINT('Ctrl Pts',(0.562916512459969,0.711513791224244,-0.324999999999856));
#5503=CARTESIAN_POINT('Ctrl Pts',(0.750555349946514,0.603180457891261,0.));
#5504=CARTESIAN_POINT('',(-0.375277674973257,0.603180457891261,-0.65));
#5505=CARTESIAN_POINT('Ctrl Pts',(-0.375277674973257,0.603180457891261,
-0.65));
#5506=CARTESIAN_POINT('Ctrl Pts',(1.66422431391311E-13,0.711513791224244,
-0.65));
#5507=CARTESIAN_POINT('Ctrl Pts',(0.375277674973257,0.603180457891261,-0.65));
#5508=CARTESIAN_POINT('Ctrl Pts',(-0.750555349946514,0.603180457891261,
-9.19165206894919E-17));
#5509=CARTESIAN_POINT('Ctrl Pts',(-0.562916512459802,0.711513791224244,
-0.325000000000144));
#5510=CARTESIAN_POINT('Ctrl Pts',(-0.375277674973257,0.603180457891261,
-0.65));
#5511=CARTESIAN_POINT('Origin',(0.375277674973257,0.,-0.65));
#5512=CARTESIAN_POINT('',(-0.375277674973257,0.,-0.65));
#5513=CARTESIAN_POINT('',(0.375277674973257,0.,-0.65));
#5514=CARTESIAN_POINT('Origin',(-0.375277674973257,0.,-0.65));
#5515=CARTESIAN_POINT('',(-0.750555349946514,0.,-9.19165206894919E-17));
#5516=CARTESIAN_POINT('Origin',(-0.750555349946514,0.,-9.19165206894919E-17));
#5517=CARTESIAN_POINT('',(-0.375277674973257,0.,0.65));
#5518=CARTESIAN_POINT('Origin',(0.,0.,0.));
#5519=CARTESIAN_POINT('',(-0.338975,0.68,4.15124648740974E-17));
#5520=CARTESIAN_POINT('Origin',(0.,0.68,0.));
#5521=CARTESIAN_POINT('',(-0.338975,0.,4.15124648740974E-17));
#5522=CARTESIAN_POINT('',(-0.338975,0.,4.15124648740974E-17));
#5523=CARTESIAN_POINT('Origin',(0.,0.,0.));
#5524=CARTESIAN_POINT('Origin',(-0.375277674973257,0.,0.65));
#5525=CARTESIAN_POINT('',(0.375277674973257,0.,0.65));
#5526=CARTESIAN_POINT('Origin',(0.750555349946514,0.,0.));
#5527=CARTESIAN_POINT('',(0.750555349946514,0.,0.));
#5528=CARTESIAN_POINT('Origin',(0.375277674973257,0.,0.65));
#5529=CARTESIAN_POINT('Origin',(0.,0.68,-1.11022302462516E-16));
#5530=CARTESIAN_POINT('Origin',(0.,0.,-1.11022302462516E-16));
#5686=UNCERTAINTY_MEASURE_WITH_UNIT(LENGTH_MEASURE(0.001),#5703,
'DISTANCE_ACCURACY_VALUE',
'Maximum model space distance between geometric entities at asserted c
onnectivities');
#5688=UNCERTAINTY_MEASURE_WITH_UNIT(LENGTH_MEASURE(0.001),#5703,
'DISTANCE_ACCURACY_VALUE',
'Maximum model space distance between geometric entities at asserted c
onnectivities');
#5700=(
GEOMETRIC_REPRESENTATION_CONTEXT(3)
GLOBAL_UNCERTAINTY_ASSIGNED_CONTEXT((#5686))
GLOBAL_UNIT_ASSIGNED_CONTEXT((#5703,#5705,#5706))
REPRESENTATION_CONTEXT('','3D')
);
#5702=(
GEOMETRIC_REPRESENTATION_CONTEXT(3)
GLOBAL_UNCERTAINTY_ASSIGNED_CONTEXT((#5688))
GLOBAL_UNIT_ASSIGNED_CONTEXT((#5703,#5705,#5706))
REPRESENTATION_CONTEXT('','3D')
);
#5703=(
LENGTH_UNIT()
NAMED_UNIT(*)
SI_UNIT(.CENTI.,.METRE.)
);
#5705=(
NAMED_UNIT(*)
PLANE_ANGLE_UNIT()
SI_UNIT($,.RADIAN.)
);
#5706=(
NAMED_UNIT(*)
SI_UNIT($,.STERADIAN.)
SOLID_ANGLE_UNIT()
);
#5718=SHAPE_DEFINITION_REPRESENTATION(#5731,#5770);
#5731=PRODUCT_DEFINITION_SHAPE('',$,#5784);
#5770=SHAPE_REPRESENTATION('',(#3672),#5700);
#5772=PRODUCT_DEFINITION_CONTEXT('part definition',#5813,'design');
#5784=PRODUCT_DEFINITION('Hex Nut - M8','Hex Nut - M8',#5797,
#5772);
#5797=PRODUCT_DEFINITION_FORMATION('',$,#5826);
#5813=APPLICATION_CONTEXT(
'Core Data for Automotive Mechanical Design Process');
#5814=PRODUCT_CONTEXT('part definition',#5813,'mechanical');
#5826=PRODUCT('Hex Nut - M8','Hex Nut - M8','Hex Nut - M8',
(#5814));
#5898=COLOUR_RGB('Black',0.12,0.14,0.17);
#5899=FILL_AREA_STYLE_COLOUR('',#5898);
#5900=FILL_AREA_STYLE('',(#5899));
#5901=SURFACE_STYLE_FILL_AREA(#5900);
#5902=SURFACE_SIDE_STYLE('',(#5901));
#5903=SURFACE_STYLE_USAGE(.BOTH.,#5902);
#5904=PRESENTATION_STYLE_ASSIGNMENT((#5903));
ENDSEC;
END-ISO-10303-21;
